ISO-10303-21;
HEADER;
FILE_DESCRIPTION (('STEP AP214'),
    '1' );
FILE_NAME ('parallel pin unhardened_iso_ISO 2338 - 2.5 m6 x 8 - St.step',
    '2026-10-06T08:51:13',
    ( '' ),
    ( '' ),
    'SwSTEP 2.0',
    'SolidWorks 2021',
    '' );
FILE_SCHEMA (( 'AUTOMOTIVE_DESIGN' ));
ENDSEC;

DATA;
#370=DIRECTION ( 'NONE',  ( 0.000000000000000000, 0.000000000000000000, 1.000000000000000000 ) ) ;
#452=EDGE_LOOP ( 'NONE', ( #21111, #56741, #113242, #114759 ) ) ;
#1104=AXIS2_PLACEMENT_3D ( 'NONE', #64324, #62193, #96206 ) ;
#1270=CARTESIAN_POINT ( 'NONE',  ( 0.000000000000000000, 0.000000000000000000, -1.142820323027524232 ) ) ;
#1938=ORIENTED_EDGE ( 'NONE', *, *, #80746, .T. ) ;
#2500=DIRECTION ( 'NONE',  ( -1.000000000000000000, -0.000000000000000000, -0.000000000000000000 ) ) ;
#2874=DIRECTION ( 'NONE',  ( 0.000000000000000000, 0.000000000000000000, 1.000000000000000000 ) ) ;
#3364=DIRECTION ( 'NONE',  ( 0.000000000000000000, 0.000000000000000000, 1.000000000000000000 ) ) ;
#5227=UNCERTAINTY_MEASURE_WITH_UNIT (LENGTH_MEASURE( 1.000000000000000082E-05 ), #53393, 'distance_accuracy_value', 'NONE');
#5836=EDGE_CURVE ( 'NONE', #100683, #75407, #110403, .T. ) ;
#7559=SHAPE_DEFINITION_REPRESENTATION ( #43228, #54265 ) ;
#8256=VERTEX_POINT ( 'NONE', #72557 ) ;
#8415=DIRECTION ( 'NONE',  ( -0.000000000000000000, 0.000000000000000000, 1.000000000000000000 ) ) ;
#8925=CARTESIAN_POINT ( 'NONE',  ( 0.000000000000000000, 0.000000000000000000, 0.000000000000000000 ) ) ;
#9207=ORIENTED_EDGE ( 'NONE', *, *, #77113, .T. ) ;
#9796=SURFACE_SIDE_STYLE ('',( #97512 ) ) ;
#10632=ORIENTED_EDGE ( 'NONE', *, *, #136286, .T. ) ;
#11207=DIRECTION ( 'NONE',  ( 0.000000000000000000, 0.000000000000000000, 1.000000000000000000 ) ) ;
#11282=SURFACE_STYLE_FILL_AREA ( #120782 ) ;
#11910=AXIS2_PLACEMENT_3D ( 'NONE', #23570, #2500, #370 ) ;
#14697=DIRECTION ( 'NONE',  ( -1.000000000000000000, -0.000000000000000000, -0.000000000000000000 ) ) ;
#15165=DIRECTION ( 'NONE',  ( -1.000000000000000000, -0.000000000000000000, -0.000000000000000000 ) ) ;
#15404=EDGE_CURVE ( 'NONE', #8256, #82515, #98851, .T. ) ;
#15603=EDGE_LOOP ( 'NONE', ( #39635, #119117, #27905, #49087 ) ) ;
#15903=AXIS2_PLACEMENT_3D ( 'NONE', #30846, #64176, #119934 ) ;
#16504=CARTESIAN_POINT ( 'NONE',  ( 0.4000000000000001887, 1.530808498934155086E-16, -1.249999999999969802 ) ) ;
#16602=EDGE_CURVE ( 'NONE', #62391, #100683, #97441, .T. ) ;
#16826=PLANE ( 'NONE',  #90423 ) ;
#16899=CARTESIAN_POINT ( 'NONE',  ( 8.000000000000007105, 0.000000000000000000, 0.000000000000000000 ) ) ;
#17844=ORIENTED_EDGE ( 'NONE', *, *, #110763, .T. ) ;
#17917=FACE_OUTER_BOUND ( 'NONE', #452, .T. ) ;
#19954=FILL_AREA_STYLE_COLOUR ( '', #122398 ) ;
#20033=CARTESIAN_POINT ( 'NONE',  ( 8.000000000000007105, 1.469576158976826708E-15, 0.000000000000000000 ) ) ;
#20034=( LENGTH_UNIT ( ) NAMED_UNIT ( * ) SI_UNIT ( .MILLI., .METRE. ) );
#20218=CONICAL_SURFACE ( 'NONE', #41146, 1.249999999999969802, 0.2617993877991415808 ) ;
#20559=EDGE_CURVE ( 'NONE', #23712, #8256, #29810, .T. ) ;
#20635=AXIS2_PLACEMENT_3D ( 'NONE', #124380, #69299, #62003 ) ;
#20974=EDGE_LOOP ( 'NONE', ( #78181, #9207, #1938, #100062 ) ) ;
#21111=ORIENTED_EDGE ( 'NONE', *, *, #114605, .T. ) ;
#21492=SURFACE_STYLE_USAGE ( .BOTH. , #98343 ) ;
#22796=DIRECTION ( 'NONE',  ( -1.000000000000000000, -0.000000000000000000, -0.000000000000000000 ) ) ;
#23570=CARTESIAN_POINT ( 'NONE',  ( 7.600000000000009415, 0.000000000000000000, 0.000000000000000000 ) ) ;
#23712=VERTEX_POINT ( 'NONE', #34125 ) ;
#24557=DIRECTION ( 'NONE',  ( 0.000000000000000000, 0.000000000000000000, 1.000000000000000000 ) ) ;
#25356=ORIENTED_EDGE ( 'NONE', *, *, #16602, .F. ) ;
#26295=DIRECTION ( 'NONE',  ( 0.000000000000000000, 0.000000000000000000, 1.000000000000000000 ) ) ;
#26990=CIRCLE ( 'NONE', #103333, 1.249999999999969802 ) ;
#27905=ORIENTED_EDGE ( 'NONE', *, *, #114605, .F. ) ;
#28491=DIRECTION ( 'NONE',  ( 1.000000000000000000, 0.000000000000000000, 0.000000000000000000 ) ) ;
#29810=CIRCLE ( 'NONE', #15903, 1.142820323027522456 ) ;
#30846=CARTESIAN_POINT ( 'NONE',  ( 8.000000000000007105, 0.000000000000000000, 0.000000000000000000 ) ) ;
#31654=DIRECTION ( 'NONE',  ( -1.000000000000000000, 0.000000000000000000, -0.000000000000000000 ) ) ;
#32432=CIRCLE ( 'NONE', #67197, 1.142820323027524232 ) ;
#33203=( GEOMETRIC_REPRESENTATION_CONTEXT ( 3 ) GLOBAL_UNCERTAINTY_ASSIGNED_CONTEXT ( ( #5227 ) ) GLOBAL_UNIT_ASSIGNED_CONTEXT ( ( #53393, #130979, #133128 ) ) REPRESENTATION_CONTEXT ( 'NONE', 'WORKASPACE' ) );
#34125=CARTESIAN_POINT ( 'NONE',  ( 8.000000000000007105, 0.000000000000000000, 1.142820323027522456 ) ) ;
#35042=AXIS2_PLACEMENT_3D ( 'NONE', #58022, #15165, #2874 ) ;
#35503=CARTESIAN_POINT ( 'NONE',  ( 0.4000000000000001887, 1.530808498934154593E-16, 1.249999999999969802 ) ) ;
#35969=CYLINDRICAL_SURFACE ( 'NONE', #20635, 1.249999999999970690 ) ;
#36857=CARTESIAN_POINT ( 'NONE',  ( 0.4000000000000001887, 0.000000000000000000, 0.000000000000000000 ) ) ;
#37076=CLOSED_SHELL ( 'NONE', ( #43315, #107423, #133130, #97814, #41546, #131185, #69596, #112026 ) ) ;
#37147=FACE_OUTER_BOUND ( 'NONE', #125644, .T. ) ;
#37392=CIRCLE ( 'NONE', #11910, 1.249999999999971578 ) ;
#37416=CARTESIAN_POINT ( 'NONE',  ( -6.349999999999999645, 0.000000000000000000, 1.249999999999970690 ) ) ;
#37922=ORIENTED_EDGE ( 'NONE', *, *, #77113, .F. ) ;
#38653=FACE_OUTER_BOUND ( 'NONE', #54206, .T. ) ;
#39635=ORIENTED_EDGE ( 'NONE', *, *, #20559, .T. ) ;
#41146=AXIS2_PLACEMENT_3D ( 'NONE', #110601, #42552, #75183 ) ;
#41449=EDGE_LOOP ( 'NONE', ( #79711, #109469, #68492, #83430 ) ) ;
#41546=ADVANCED_FACE ( 'NONE', ( #107058 ), #41812, .F. ) ;
#41812=PLANE ( 'NONE',  #46635 ) ;
#41813=PRESENTATION_STYLE_ASSIGNMENT (( #21492 ) ) ;
#42552=DIRECTION ( 'NONE',  ( 1.000000000000000000, 0.000000000000000000, 0.000000000000000000 ) ) ;
#43167=FILL_AREA_STYLE ('',( #19954 ) ) ;
#43228=PRODUCT_DEFINITION_SHAPE ( 'NONE', 'NONE',  #46631 ) ;
#43315=ADVANCED_FACE ( 'NONE', ( #59017 ), #121433, .T. ) ;
#43960=( NAMED_UNIT ( * ) PLANE_ANGLE_UNIT ( ) SI_UNIT ( $, .RADIAN. ) );
#46631=PRODUCT_DEFINITION ( 'UNKNOWN', '', #93384, #135774 ) ;
#46635=AXIS2_PLACEMENT_3D ( 'NONE', #20033, #31654, #8415 ) ;
#47311=CARTESIAN_POINT ( 'NONE',  ( 7.600000000000009415, 1.530808498934156811E-16, -1.249999999999971578 ) ) ;
#47617=LINE ( 'NONE', #37416, #109591 ) ;
#48097=DIRECTION ( 'NONE',  ( 0.000000000000000000, 0.000000000000000000, -1.000000000000000000 ) ) ;
#48941=EDGE_LOOP ( 'NONE', ( #123439, #117648, #10632, #25356 ) ) ;
#49087=ORIENTED_EDGE ( 'NONE', *, *, #110763, .F. ) ;
#49433=AXIS2_PLACEMENT_3D ( 'NONE', #136205, #111612, #81138 ) ;
#51673=CARTESIAN_POINT ( 'NONE',  ( 7.600000000000009415, 0.000000000000000000, 1.249999999999971578 ) ) ;
#51688=CONICAL_SURFACE ( 'NONE', #49433, 1.142820323027522456, 0.2617993877991512952 ) ;
#53195=DIRECTION ( 'NONE',  ( 1.000000000000000000, 0.000000000000000000, 0.000000000000000000 ) ) ;
#53207=DIRECTION ( 'NONE',  ( -0.9659258262890677571, 3.169619151431787128E-17, -0.2588190451025225713 ) ) ;
#53299=( LENGTH_UNIT ( ) NAMED_UNIT ( * ) SI_UNIT ( .MILLI., .METRE. ) );
#53393=( LENGTH_UNIT ( ) NAMED_UNIT ( * ) SI_UNIT ( .MILLI., .METRE. ) );
#54206=EDGE_LOOP ( 'NONE', ( #112118, #123161, #17844, #37922 ) ) ;
#54265=SHAPE_REPRESENTATION ( 'parallel pin unhardened_iso_ISO 2338 - 2.5 m6 x 8 - St', ( #127880 ), #33203 ) ;
#56020=PRODUCT ( 'parallel pin unhardened_iso_ISO 2338 - 2.5 m6 x 8 - St', 'parallel pin unhardened_iso_ISO 2338 - 2.5 m6 x 8 - St', '', ( #71423 ) ) ;
#56287=VECTOR ( 'NONE', #75029, 1000.000000000000000 ) ;
#56741=ORIENTED_EDGE ( 'NONE', *, *, #129645, .T. ) ;
#57555=DIRECTION ( 'NONE',  ( 0.000000000000000000, 0.000000000000000000, 1.000000000000000000 ) ) ;
#57807=APPLICATION_CONTEXT ( 'automotive_design' ) ;
#58022=CARTESIAN_POINT ( 'NONE',  ( 0.000000000000000000, 0.000000000000000000, 0.000000000000000000 ) ) ;
#59017=FACE_OUTER_BOUND ( 'NONE', #48941, .T. ) ;
#60948=COLOUR_RGB ( '', 0.31764706, 0.68627451, 0.89019608) ;
#61102=CARTESIAN_POINT ( 'NONE',  ( 0.000000000000000000, 1.142820323027524232, 0.000000000000000000 ) ) ;
#61849=DIRECTION ( 'NONE',  ( -1.000000000000000000, -0.000000000000000000, -0.000000000000000000 ) ) ;
#62003=DIRECTION ( 'NONE',  ( 0.000000000000000000, 0.000000000000000000, 1.000000000000000000 ) ) ;
#62193=DIRECTION ( 'NONE',  ( -1.000000000000000000, -0.000000000000000000, -0.000000000000000000 ) ) ;
#62391=VERTEX_POINT ( 'NONE', #1270 ) ;
#62803=EDGE_LOOP ( 'NONE', ( #116910, #86416 ) ) ;
#63513=SURFACE_STYLE_USAGE ( .BOTH. , #9796 ) ;
#63548=DIRECTION ( 'NONE',  ( -1.000000000000000000, -0.000000000000000000, -0.000000000000000000 ) ) ;
#63639=CYLINDRICAL_SURFACE ( 'NONE', #1104, 1.249999999999970690 ) ;
#64176=DIRECTION ( 'NONE',  ( -1.000000000000000000, -0.000000000000000000, -0.000000000000000000 ) ) ;
#64324=CARTESIAN_POINT ( 'NONE',  ( -6.349999999999999645, 0.000000000000000000, 0.000000000000000000 ) ) ;
#66995=ORIENTED_EDGE ( 'NONE', *, *, #75484, .T. ) ;
#67197=AXIS2_PLACEMENT_3D ( 'NONE', #134646, #99850, #3364 ) ;
#68492=ORIENTED_EDGE ( 'NONE', *, *, #16602, .T. ) ;
#69299=DIRECTION ( 'NONE',  ( -1.000000000000000000, -0.000000000000000000, -0.000000000000000000 ) ) ;
#69596=ADVANCED_FACE ( 'NONE', ( #80192 ), #35969, .T. ) ;
#70432=VERTEX_POINT ( 'NONE', #51673 ) ;
#71241=CARTESIAN_POINT ( 'NONE',  ( 0.4000000000000001887, 0.000000000000000000, 0.000000000000000000 ) ) ;
#71423=PRODUCT_CONTEXT ( 'NONE', #106872, 'mechanical' ) ;
#72533=CONICAL_SURFACE ( 'NONE', #91038, 1.142820323027522456, 0.2617993877991512952 ) ;
#72557=CARTESIAN_POINT ( 'NONE',  ( 8.000000000000007105, 1.465179874765178344E-16, -1.142820323027522456 ) ) ;
#73642=( NAMED_UNIT ( * ) PLANE_ANGLE_UNIT ( ) SI_UNIT ( $, .RADIAN. ) );
#74405=CARTESIAN_POINT ( 'NONE',  ( -6.349999999999999645, 1.530808498934155579E-16, -1.249999999999970690 ) ) ;
#75029=DIRECTION ( 'NONE',  ( 0.9659258262890703106, 0.000000000000000000, -0.2588190451025131900 ) ) ;
#75183=DIRECTION ( 'NONE',  ( 0.000000000000000000, 0.000000000000000000, -1.000000000000000000 ) ) ;
#75407=VERTEX_POINT ( 'NONE', #107841 ) ;
#75484=EDGE_CURVE ( 'NONE', #100092, #62391, #32432, .T. ) ;
#75721=CARTESIAN_POINT ( 'NONE',  ( 0.4000000000000001887, 0.000000000000000000, -1.249999999999969802 ) ) ;
#75875=( NAMED_UNIT ( * ) SI_UNIT ( $, .STERADIAN. ) SOLID_ANGLE_UNIT ( ) );
#76868=EDGE_CURVE ( 'NONE', #62391, #100092, #92841, .T. ) ;
#77113=EDGE_CURVE ( 'NONE', #82515, #70432, #37392, .T. ) ;
#77733=ADVANCED_BREP_SHAPE_REPRESENTATION ( '', ( #94738, #127880 ), #33203 ) ;
#78181=ORIENTED_EDGE ( 'NONE', *, *, #129645, .F. ) ;
#78786=DIRECTION ( 'NONE',  ( -1.000000000000000000, -0.000000000000000000, -0.000000000000000000 ) ) ;
#79711=ORIENTED_EDGE ( 'NONE', *, *, #81637, .F. ) ;
#79736=DIRECTION ( 'NONE',  ( 0.9659258262890703106, 3.169619151431672497E-17, 0.2588190451025131900 ) ) ;
#80192=FACE_OUTER_BOUND ( 'NONE', #20974, .T. ) ;
#80731=DIRECTION ( 'NONE',  ( -1.000000000000000000, -0.000000000000000000, -0.000000000000000000 ) ) ;
#80746=EDGE_CURVE ( 'NONE', #70432, #75407, #47617, .T. ) ;
#81138=DIRECTION ( 'NONE',  ( 0.000000000000000000, 0.000000000000000000, 1.000000000000000000 ) ) ;
#81637=EDGE_CURVE ( 'NONE', #100092, #75407, #136192, .T. ) ;
#82515=VERTEX_POINT ( 'NONE', #47311 ) ;
#82884=DIRECTION ( 'NONE',  ( 0.000000000000000000, 0.000000000000000000, 1.000000000000000000 ) ) ;
#83216=EDGE_CURVE ( 'NONE', #8256, #23712, #97219, .T. ) ;
#83266=CIRCLE ( 'NONE', #143476, 1.249999999999971578 ) ;
#83430=ORIENTED_EDGE ( 'NONE', *, *, #5836, .T. ) ;
#83554=UNCERTAINTY_MEASURE_WITH_UNIT (LENGTH_MEASURE( 1.000000000000000082E-05 ), #20034, 'distance_accuracy_value', 'NONE');
#85271=DIRECTION ( 'NONE',  ( -0.9659258262890677571, 0.000000000000000000, 0.2588190451025225713 ) ) ;
#86377=( GEOMETRIC_REPRESENTATION_CONTEXT ( 3 ) GLOBAL_UNCERTAINTY_ASSIGNED_CONTEXT ( ( #83554 ) ) GLOBAL_UNIT_ASSIGNED_CONTEXT ( ( #20034, #43960, #75875 ) ) REPRESENTATION_CONTEXT ( 'NONE', 'WORKASPACE' ) );
#86416=ORIENTED_EDGE ( 'NONE', *, *, #83216, .F. ) ;
#88179=SHAPE_REPRESENTATION_RELATIONSHIP ( 'NONE' , 'NONE' ,  #54265, #77733 ) ;
#89437=CARTESIAN_POINT ( 'NONE',  ( 7.600000000000009415, 0.000000000000000000, 0.000000000000000000 ) ) ;
#90423=AXIS2_PLACEMENT_3D ( 'NONE', #61102, #126297, #103799 ) ;
#91038=AXIS2_PLACEMENT_3D ( 'NONE', #16899, #61849, #82884 ) ;
#92685=AXIS2_PLACEMENT_3D ( 'NONE', #122135, #22796, #11207 ) ;
#92841=CIRCLE ( 'NONE', #35042, 1.142820323027524232 ) ;
#93287=STYLED_ITEM ( 'NONE', ( #41813 ), #77733 ) ;
#93384=PRODUCT_DEFINITION_FORMATION_WITH_SPECIFIED_SOURCE ( 'ANY', '', #56020, .NOT_KNOWN. ) ;
#94738=MANIFOLD_SOLID_BREP ( 'Base-Revolve', #37076 ) ;
#96206=DIRECTION ( 'NONE',  ( 0.000000000000000000, 0.000000000000000000, 1.000000000000000000 ) ) ;
#96685=CARTESIAN_POINT ( 'NONE',  ( 8.000000000000007105, 1.399551250596199630E-16, -1.142820323027522456 ) ) ;
#97219=CIRCLE ( 'NONE', #92685, 1.142820323027522456 ) ;
#97441=LINE ( 'NONE', #75721, #56287 ) ;
#97462=ORIENTED_EDGE ( 'NONE', *, *, #76868, .T. ) ;
#97512=SURFACE_STYLE_FILL_AREA ( #43167 ) ;
#97814=ADVANCED_FACE ( 'NONE', ( #37147 ), #16826, .F. ) ;
#98255=( NAMED_UNIT ( * ) SI_UNIT ( $, .STERADIAN. ) SOLID_ANGLE_UNIT ( ) );
#98343=SURFACE_SIDE_STYLE ('',( #11282 ) ) ;
#98851=LINE ( 'NONE', #96685, #116035 ) ;
#99850=DIRECTION ( 'NONE',  ( -1.000000000000000000, -0.000000000000000000, -0.000000000000000000 ) ) ;
#100062=ORIENTED_EDGE ( 'NONE', *, *, #5836, .F. ) ;
#100092=VERTEX_POINT ( 'NONE', #135633 ) ;
#100683=VERTEX_POINT ( 'NONE', #16504 ) ;
#102489=CARTESIAN_POINT ( 'NONE',  ( 0.4000000000000001887, 0.000000000000000000, 0.000000000000000000 ) ) ;
#102854=DIRECTION ( 'NONE',  ( -1.000000000000000000, -0.000000000000000000, -0.000000000000000000 ) ) ;
#103333=AXIS2_PLACEMENT_3D ( 'NONE', #71241, #14697, #26295 ) ;
#103799=DIRECTION ( 'NONE',  ( 0.000000000000000000, 0.000000000000000000, -1.000000000000000000 ) ) ;
#106872=APPLICATION_CONTEXT ( 'automotive_design' ) ;
#107058=FACE_OUTER_BOUND ( 'NONE', #62803, .T. ) ;
#107423=ADVANCED_FACE ( 'NONE', ( #17917 ), #63639, .T. ) ;
#107841=CARTESIAN_POINT ( 'NONE',  ( 0.4000000000000001887, 0.000000000000000000, 1.249999999999969802 ) ) ;
#108443=FACE_OUTER_BOUND ( 'NONE', #41449, .T. ) ;
#108446=FILL_AREA_STYLE_COLOUR ( '', #60948 ) ;
#109220=VECTOR ( 'NONE', #63548, 1000.000000000000000 ) ;
#109469=ORIENTED_EDGE ( 'NONE', *, *, #76868, .F. ) ;
#109591=VECTOR ( 'NONE', #78786, 1000.000000000000000 ) ;
#110403=CIRCLE ( 'NONE', #128946, 1.249999999999969802 ) ;
#110601=CARTESIAN_POINT ( 'NONE',  ( 0.4000000000000001887, 0.000000000000000000, 0.000000000000000000 ) ) ;
#110763=EDGE_CURVE ( 'NONE', #23712, #70432, #140381, .T. ) ;
#111612=DIRECTION ( 'NONE',  ( -1.000000000000000000, -0.000000000000000000, -0.000000000000000000 ) ) ;
#112026=ADVANCED_FACE ( 'NONE', ( #108443 ), #20218, .T. ) ;
#112118=ORIENTED_EDGE ( 'NONE', *, *, #15404, .F. ) ;
#113189=MECHANICAL_DESIGN_GEOMETRIC_PRESENTATION_REPRESENTATION('',(#127064),#141030);
#113242=ORIENTED_EDGE ( 'NONE', *, *, #136286, .F. ) ;
#114130=UNCERTAINTY_MEASURE_WITH_UNIT (LENGTH_MEASURE( 1.000000000000000082E-05 ), #53299, 'distance_accuracy_value', 'NONE');
#114605=EDGE_CURVE ( 'NONE', #70432, #82515, #83266, .T. ) ;
#114759=ORIENTED_EDGE ( 'NONE', *, *, #80746, .F. ) ;
#116035=VECTOR ( 'NONE', #53207, 1000.000000000000227 ) ;
#116910=ORIENTED_EDGE ( 'NONE', *, *, #20559, .F. ) ;
#117153=LINE ( 'NONE', #74405, #109220 ) ;
#117648=ORIENTED_EDGE ( 'NONE', *, *, #81637, .T. ) ;
#119117=ORIENTED_EDGE ( 'NONE', *, *, #15404, .T. ) ;
#119263=PRESENTATION_STYLE_ASSIGNMENT (( #63513 ) ) ;
#119934=DIRECTION ( 'NONE',  ( 0.000000000000000000, 0.000000000000000000, 1.000000000000000000 ) ) ;
#120782=FILL_AREA_STYLE ('',( #108446 ) ) ;
#121433=CONICAL_SURFACE ( 'NONE', #139987, 1.249999999999969802, 0.2617993877991415808 ) ;
#122135=CARTESIAN_POINT ( 'NONE',  ( 8.000000000000007105, 0.000000000000000000, 0.000000000000000000 ) ) ;
#122398=COLOUR_RGB ( '', 0.31764706, 0.68627451, 0.89019608) ;
#123161=ORIENTED_EDGE ( 'NONE', *, *, #83216, .T. ) ;
#123439=ORIENTED_EDGE ( 'NONE', *, *, #75484, .F. ) ;
#124380=CARTESIAN_POINT ( 'NONE',  ( -6.349999999999999645, 0.000000000000000000, 0.000000000000000000 ) ) ;
#125644=EDGE_LOOP ( 'NONE', ( #97462, #66995 ) ) ;
#125699=MECHANICAL_DESIGN_GEOMETRIC_PRESENTATION_REPRESENTATION('',(#93287),#86377);
#126297=DIRECTION ( 'NONE',  ( 1.000000000000000000, 0.000000000000000000, 0.000000000000000000 ) ) ;
#127064=STYLED_ITEM ( 'NONE', ( #119263 ), #94738 ) ;
#127880=AXIS2_PLACEMENT_3D ( 'NONE', #8925, #141658, #53195 ) ;
#128946=AXIS2_PLACEMENT_3D ( 'NONE', #36857, #102854, #24557 ) ;
#129645=EDGE_CURVE ( 'NONE', #82515, #100683, #117153, .T. ) ;
#130979=( NAMED_UNIT ( * ) PLANE_ANGLE_UNIT ( ) SI_UNIT ( $, .RADIAN. ) );
#131185=ADVANCED_FACE ( 'NONE', ( #38653 ), #72533, .T. ) ;
#132922=VECTOR ( 'NONE', #79736, 1000.000000000000000 ) ;
#133128=( NAMED_UNIT ( * ) SI_UNIT ( $, .STERADIAN. ) SOLID_ANGLE_UNIT ( ) );
#133130=ADVANCED_FACE ( 'NONE', ( #135516 ), #51688, .T. ) ;
#134646=CARTESIAN_POINT ( 'NONE',  ( 0.000000000000000000, 0.000000000000000000, 0.000000000000000000 ) ) ;
#135516=FACE_OUTER_BOUND ( 'NONE', #15603, .T. ) ;
#135633=CARTESIAN_POINT ( 'NONE',  ( 0.000000000000000000, 1.465179874765178344E-16, 1.142820323027524232 ) ) ;
#135756=VECTOR ( 'NONE', #85271, 1000.000000000000227 ) ;
#135774=PRODUCT_DEFINITION_CONTEXT ( 'detailed design', #57807, 'design' ) ;
#136192=LINE ( 'NONE', #35503, #132922 ) ;
#136205=CARTESIAN_POINT ( 'NONE',  ( 8.000000000000007105, 0.000000000000000000, 0.000000000000000000 ) ) ;
#136286=EDGE_CURVE ( 'NONE', #75407, #100683, #26990, .T. ) ;
#138251=CARTESIAN_POINT ( 'NONE',  ( 8.000000000000007105, 0.000000000000000000, 1.142820323027522456 ) ) ;
#139987=AXIS2_PLACEMENT_3D ( 'NONE', #102489, #28491, #48097 ) ;
#140381=LINE ( 'NONE', #138251, #135756 ) ;
#141030=( GEOMETRIC_REPRESENTATION_CONTEXT ( 3 ) GLOBAL_UNCERTAINTY_ASSIGNED_CONTEXT ( ( #114130 ) ) GLOBAL_UNIT_ASSIGNED_CONTEXT ( ( #53299, #73642, #98255 ) ) REPRESENTATION_CONTEXT ( 'NONE', 'WORKASPACE' ) );
#141658=DIRECTION ( 'NONE',  ( 0.000000000000000000, 0.000000000000000000, 1.000000000000000000 ) ) ;
#143476=AXIS2_PLACEMENT_3D ( 'NONE', #89437, #80731, #57555 ) ;
ENDSEC;
END-ISO-10303-21;
